ISO-10303-21;
HEADER;
/* Generated by software containing ST-Developer
 * from STEP Tools, Inc. (www.steptools.com) 
 */

FILE_DESCRIPTION(
/* description */ ('Rigid flange shaft coupling assembly'),
/* implementation_level */ '2;1');

FILE_NAME(
/* name */ 'Mounting bush (3).step',
/* time_stamp */ '2026-10-27T10:47:16-07:00',
/* author */ (''),
/* organization */ (''),
/* preprocessor_version */ 'ST-DEVELOPER v20.2',
/* originating_system */ 'Autodesk Translation Framework v15.17.0.0',
/* authorisation */ '');

FILE_SCHEMA (('AUTOMOTIVE_DESIGN { 1 0 10303 214 3 1 1 }'));
ENDSEC;

DATA;
#10=MECHANICAL_DESIGN_GEOMETRIC_PRESENTATION_REPRESENTATION('',(#406),#9141);
#350=SHAPE_REPRESENTATION_RELATIONSHIP('SRR','None',#9284,#378);
#378=ADVANCED_BREP_SHAPE_REPRESENTATION('',(#435),#9119);
#406=STYLED_ITEM('',(#9493),#435);
#435=MANIFOLD_SOLID_BREP('Body1',#4760);
#483=FACE_BOUND('',#1103,.T.);
#484=FACE_BOUND('',#1105,.T.);
#606=PLANE('',#5200);
#607=PLANE('',#5201);
#798=FACE_OUTER_BOUND('',#1100,.T.);
#799=FACE_OUTER_BOUND('',#1101,.T.);
#800=FACE_OUTER_BOUND('',#1102,.T.);
#801=FACE_OUTER_BOUND('',#1104,.T.);
#1100=EDGE_LOOP('',(#3471,#3472,#3473,#3474));
#1101=EDGE_LOOP('',(#3475,#3476,#3477,#3478));
#1102=EDGE_LOOP('',(#3479));
#1103=EDGE_LOOP('',(#3480));
#1104=EDGE_LOOP('',(#3481));
#1105=EDGE_LOOP('',(#3482));
#1483=LINE('',#7344,#1828);
#1484=LINE('',#7350,#1829);
#1828=VECTOR('',#5926,0.425);
#1829=VECTOR('',#5933,0.645);
#2131=CIRCLE('',#5195,0.425);
#2132=CIRCLE('',#5196,0.425);
#2133=CIRCLE('',#5198,0.645);
#2134=CIRCLE('',#5199,0.645);
#2352=VERTEX_POINT('',#7341);
#2353=VERTEX_POINT('',#7343);
#2354=VERTEX_POINT('',#7347);
#2355=VERTEX_POINT('',#7349);
#2779=EDGE_CURVE('',#2352,#2352,#2131,.T.);
#2780=EDGE_CURVE('',#2352,#2353,#1483,.T.);
#2781=EDGE_CURVE('',#2353,#2353,#2132,.T.);
#2782=EDGE_CURVE('',#2354,#2354,#2133,.T.);
#2783=EDGE_CURVE('',#2354,#2355,#1484,.T.);
#2784=EDGE_CURVE('',#2355,#2355,#2134,.T.);
#3471=ORIENTED_EDGE('',*,*,#2779,.F.);
#3472=ORIENTED_EDGE('',*,*,#2780,.T.);
#3473=ORIENTED_EDGE('',*,*,#2781,.T.);
#3474=ORIENTED_EDGE('',*,*,#2780,.F.);
#3475=ORIENTED_EDGE('',*,*,#2782,.F.);
#3476=ORIENTED_EDGE('',*,*,#2783,.T.);
#3477=ORIENTED_EDGE('',*,*,#2784,.T.);
#3478=ORIENTED_EDGE('',*,*,#2783,.F.);
#3479=ORIENTED_EDGE('',*,*,#2782,.T.);
#3480=ORIENTED_EDGE('',*,*,#2779,.T.);
#3481=ORIENTED_EDGE('',*,*,#2784,.F.);
#3482=ORIENTED_EDGE('',*,*,#2781,.F.);
#4417=CYLINDRICAL_SURFACE('',#5194,0.425);
#4418=CYLINDRICAL_SURFACE('',#5197,0.645);
#4534=ADVANCED_FACE('',(#798),#4417,.F.);
#4535=ADVANCED_FACE('',(#799),#4418,.T.);
#4536=ADVANCED_FACE('',(#800,#483),#606,.T.);
#4537=ADVANCED_FACE('',(#801,#484),#607,.F.);
#4760=CLOSED_SHELL('',(#4534,#4535,#4536,#4537));
#5193=AXIS2_PLACEMENT_3D('',#7339,#5920,#5921);
#5194=AXIS2_PLACEMENT_3D('',#7340,#5922,#5923);
#5195=AXIS2_PLACEMENT_3D('',#7342,#5924,#5925);
#5196=AXIS2_PLACEMENT_3D('',#7345,#5927,#5928);
#5197=AXIS2_PLACEMENT_3D('',#7346,#5929,#5930);
#5198=AXIS2_PLACEMENT_3D('',#7348,#5931,#5932);
#5199=AXIS2_PLACEMENT_3D('',#7351,#5934,#5935);
#5200=AXIS2_PLACEMENT_3D('',#7352,#5936,#5937);
#5201=AXIS2_PLACEMENT_3D('',#7353,#5938,#5939);
#5920=DIRECTION('axis',(0.,0.,1.));
#5921=DIRECTION('refdir',(1.,0.,0.));
#5922=DIRECTION('center_axis',(0.,0.,1.));
#5923=DIRECTION('ref_axis',(1.,0.,0.));
#5924=DIRECTION('center_axis',(0.,0.,-1.));
#5925=DIRECTION('ref_axis',(1.,0.,0.));
#5926=DIRECTION('',(0.,0.,-1.));
#5927=DIRECTION('center_axis',(0.,0.,-1.));
#5928=DIRECTION('ref_axis',(1.,0.,0.));
#5929=DIRECTION('center_axis',(0.,0.,1.));
#5930=DIRECTION('ref_axis',(1.,0.,0.));
#5931=DIRECTION('center_axis',(0.,0.,1.));
#5932=DIRECTION('ref_axis',(1.,0.,0.));
#5933=DIRECTION('',(0.,0.,-1.));
#5934=DIRECTION('center_axis',(0.,0.,1.));
#5935=DIRECTION('ref_axis',(1.,0.,0.));
#5936=DIRECTION('center_axis',(0.,0.,1.));
#5937=DIRECTION('ref_axis',(1.,0.,0.));
#5938=DIRECTION('center_axis',(0.,0.,1.));
#5939=DIRECTION('ref_axis',(1.,0.,0.));
#7339=CARTESIAN_POINT('',(0.,0.,0.));
#7340=CARTESIAN_POINT('Origin',(4.75,20.,3.2));
#7341=CARTESIAN_POINT('',(4.325,20.,4.4));
#7342=CARTESIAN_POINT('Origin',(4.75,20.,4.4));
#7343=CARTESIAN_POINT('',(4.325,20.,3.2));
#7344=CARTESIAN_POINT('',(4.325,20.,3.2));
#7345=CARTESIAN_POINT('Origin',(4.75,20.,3.2));
#7346=CARTESIAN_POINT('Origin',(4.75,20.,3.2));
#7347=CARTESIAN_POINT('',(4.105,20.,4.4));
#7348=CARTESIAN_POINT('Origin',(4.75,20.,4.4));
#7349=CARTESIAN_POINT('',(4.105,20.,3.2));
#7350=CARTESIAN_POINT('',(4.105,20.,3.2));
#7351=CARTESIAN_POINT('Origin',(4.75,20.,3.2));
#7352=CARTESIAN_POINT('Origin',(4.75,20.,4.4));
#7353=CARTESIAN_POINT('Origin',(4.75,20.,3.2));
#9086=UNCERTAINTY_MEASURE_WITH_UNIT(LENGTH_MEASURE(0.001),#9142,
'DISTANCE_ACCURACY_VALUE',
'Maximum model space distance between geometric entities at asserted c
onnectivities');
#9108=UNCERTAINTY_MEASURE_WITH_UNIT(LENGTH_MEASURE(0.001),#9142,
'DISTANCE_ACCURACY_VALUE',
'Maximum model space distance between geometric entities at asserted c
onnectivities');
#9119=(
GEOMETRIC_REPRESENTATION_CONTEXT(3)
GLOBAL_UNCERTAINTY_ASSIGNED_CONTEXT((#9086))
GLOBAL_UNIT_ASSIGNED_CONTEXT((#9142,#9144,#9145))
REPRESENTATION_CONTEXT('','3D')
);
#9141=(
GEOMETRIC_REPRESENTATION_CONTEXT(3)
GLOBAL_UNCERTAINTY_ASSIGNED_CONTEXT((#9108))
GLOBAL_UNIT_ASSIGNED_CONTEXT((#9142,#9144,#9145))
REPRESENTATION_CONTEXT('','3D')
);
#9142=(
LENGTH_UNIT()
NAMED_UNIT(*)
SI_UNIT(.CENTI.,.METRE.)
);
#9144=(
NAMED_UNIT(*)
PLANE_ANGLE_UNIT()
SI_UNIT($,.RADIAN.)
);
#9145=(
NAMED_UNIT(*)
SI_UNIT($,.STERADIAN.)
SOLID_ANGLE_UNIT()
);
#9156=SHAPE_DEFINITION_REPRESENTATION(#9188,#9284);
#9188=PRODUCT_DEFINITION_SHAPE('',$,#9317);
#9284=SHAPE_REPRESENTATION('',(#5193),#9119);
#9306=PRODUCT_DEFINITION_CONTEXT('part definition',#9404,'design');
#9317=PRODUCT_DEFINITION('Mounting bush (3)','Mounting bush (3)',#9349,#9306);
#9349=PRODUCT_DEFINITION_FORMATION('',$,#9416);
#9404=APPLICATION_CONTEXT(
'Core Data for Automotive Mechanical Design Process');
#9405=PRODUCT_CONTEXT('part definition',#9404,'mechanical');
#9416=PRODUCT('Mounting bush (3)','Mounting bush (3)','Mounting bush (3)',(#9405));
#9487=COLOUR_RGB('Sky Blue',0.24,0.69,0.87);
#9488=FILL_AREA_STYLE_COLOUR('',#9487);
#9489=FILL_AREA_STYLE('',(#9488));
#9490=SURFACE_STYLE_FILL_AREA(#9489);
#9491=SURFACE_SIDE_STYLE('',(#9490));
#9492=SURFACE_STYLE_USAGE(.BOTH.,#9491);
#9493=PRESENTATION_STYLE_ASSIGNMENT((#9492));
ENDSEC;
END-ISO-10303-21;
